ISO-10303-21;
HEADER;
/* Generated by software containing ST-Developer
 * from STEP Tools, Inc. (www.steptools.com) 
 */

FILE_DESCRIPTION(
/* description */ ('Four-bar parallelogram arm'),
/* implementation_level */ '2;1');

FILE_NAME(
/* name */ 'Cap Screw - M4x16.step',
/* time_stamp */ '2026-10-28T03:24:55-07:00',
/* author */ (''),
/* organization */ (''),
/* preprocessor_version */ 'ST-DEVELOPER v20.2',
/* originating_system */ 'Autodesk Translation Framework v15.17.0.0',
/* authorisation */ '');

FILE_SCHEMA (('AUTOMOTIVE_DESIGN { 1 0 10303 214 3 1 1 }'));
ENDSEC;

DATA;
#10=MECHANICAL_DESIGN_GEOMETRIC_PRESENTATION_REPRESENTATION('',(#679),#14512);
#487=CONICAL_SURFACE('',#8895,0.325,0.785398163397448);
#488=CONICAL_SURFACE('',#8899,0.335,0.785398163397448);
#489=CONICAL_SURFACE('',#8903,0.21,0.463647609000806);
#490=CONICAL_SURFACE('',#8907,0.18,0.785398163397448);
#493=ORIENTED_CLOSED_SHELL('',*,#7386,.F.);
#496=BREP_WITH_VOIDS('Body1',#7385,(#493));
#571=SHAPE_REPRESENTATION_RELATIONSHIP('SRR','None',#14796,#621);
#621=ADVANCED_BREP_SHAPE_REPRESENTATION('',(#496),#14511);
#679=STYLED_ITEM('',(#15094),#496);
#1005=FACE_BOUND('',#2299,.T.);
#1190=PLANE('',#8893);
#1191=PLANE('',#8901);
#1192=PLANE('',#8909);
#1193=PLANE('',#8910);
#1194=PLANE('',#8911);
#1195=PLANE('',#8912);
#1196=PLANE('',#8913);
#1197=PLANE('',#8914);
#1198=PLANE('',#8915);
#1199=PLANE('',#8916);
#1200=PLANE('',#8917);
#1604=FACE_OUTER_BOUND('',#2294,.T.);
#1605=FACE_OUTER_BOUND('',#2295,.T.);
#1606=FACE_OUTER_BOUND('',#2296,.T.);
#1607=FACE_OUTER_BOUND('',#2297,.T.);
#1608=FACE_OUTER_BOUND('',#2298,.T.);
#1609=FACE_OUTER_BOUND('',#2300,.T.);
#1610=FACE_OUTER_BOUND('',#2301,.T.);
#1611=FACE_OUTER_BOUND('',#2302,.T.);
#1612=FACE_OUTER_BOUND('',#2303,.T.);
#1613=FACE_OUTER_BOUND('',#2304,.T.);
#1614=FACE_OUTER_BOUND('',#2305,.T.);
#1615=FACE_OUTER_BOUND('',#2306,.T.);
#1616=FACE_OUTER_BOUND('',#2307,.T.);
#1617=FACE_OUTER_BOUND('',#2308,.T.);
#1618=FACE_OUTER_BOUND('',#2309,.T.);
#1619=FACE_OUTER_BOUND('',#2310,.T.);
#1620=FACE_OUTER_BOUND('',#2311,.T.);
#2294=EDGE_LOOP('',(#6650));
#2295=EDGE_LOOP('',(#6651,#6652,#6653,#6654));
#2296=EDGE_LOOP('',(#6655,#6656,#6657,#6658));
#2297=EDGE_LOOP('',(#6659,#6660,#6661,#6662));
#2298=EDGE_LOOP('',(#6663));
#2299=EDGE_LOOP('',(#6664));
#2300=EDGE_LOOP('',(#6665,#6666,#6667,#6668));
#2301=EDGE_LOOP('',(#6669,#6670,#6671,#6672));
#2302=EDGE_LOOP('',(#6673,#6674,#6675,#6676));
#2303=EDGE_LOOP('',(#6677));
#2304=EDGE_LOOP('',(#6678,#6679,#6680,#6681));
#2305=EDGE_LOOP('',(#6682,#6683,#6684,#6685));
#2306=EDGE_LOOP('',(#6686,#6687,#6688,#6689));
#2307=EDGE_LOOP('',(#6690,#6691,#6692,#6693));
#2308=EDGE_LOOP('',(#6694,#6695,#6696,#6697));
#2309=EDGE_LOOP('',(#6698,#6699,#6700,#6701));
#2310=EDGE_LOOP('',(#6702,#6703,#6704,#6705,#6706,#6707));
#2311=EDGE_LOOP('',(#6708,#6709,#6710,#6711,#6712,#6713));
#2682=LINE('',#14284,#3076);
#2683=LINE('',#14288,#3077);
#2684=LINE('',#14292,#3078);
#2685=LINE('',#14299,#3079);
#2686=LINE('',#14303,#3080);
#2687=LINE('',#14307,#3081);
#2688=LINE('',#14312,#3082);
#2689=LINE('',#14314,#3083);
#2690=LINE('',#14316,#3084);
#2691=LINE('',#14317,#3085);
#2692=LINE('',#14320,#3086);
#2693=LINE('',#14322,#3087);
#2694=LINE('',#14323,#3088);
#2695=LINE('',#14326,#3089);
#2696=LINE('',#14328,#3090);
#2697=LINE('',#14329,#3091);
#2698=LINE('',#14332,#3092);
#2699=LINE('',#14334,#3093);
#2700=LINE('',#14335,#3094);
#2701=LINE('',#14338,#3095);
#2702=LINE('',#14340,#3096);
#2703=LINE('',#14341,#3097);
#2704=LINE('',#14343,#3098);
#2705=LINE('',#14344,#3099);
#3076=VECTOR('',#11258,0.325);
#3077=VECTOR('',#11263,0.35);
#3078=VECTOR('',#11268,0.335);
#3079=VECTOR('',#11277,0.21);
#3080=VECTOR('',#11282,0.2);
#3081=VECTOR('',#11287,0.18);
#3082=VECTOR('',#11292,1.);
#3083=VECTOR('',#11293,1.);
#3084=VECTOR('',#11294,1.);
#3085=VECTOR('',#11295,1.);
#3086=VECTOR('',#11298,1.);
#3087=VECTOR('',#11299,1.);
#3088=VECTOR('',#11300,1.);
#3089=VECTOR('',#11303,1.);
#3090=VECTOR('',#11304,1.);
#3091=VECTOR('',#11305,1.);
#3092=VECTOR('',#11308,1.);
#3093=VECTOR('',#11309,1.);
#3094=VECTOR('',#11310,1.);
#3095=VECTOR('',#11313,1.);
#3096=VECTOR('',#11314,1.);
#3097=VECTOR('',#11315,1.);
#3098=VECTOR('',#11318,1.);
#3099=VECTOR('',#11319,1.);
#3537=CIRCLE('',#8894,0.3);
#3538=CIRCLE('',#8896,0.35);
#3539=CIRCLE('',#8898,0.35);
#3540=CIRCLE('',#8900,0.32);
#3541=CIRCLE('',#8902,0.22);
#3542=CIRCLE('',#8904,0.1954);
#3543=CIRCLE('',#8906,0.1954);
#3544=CIRCLE('',#8908,0.16);
#4105=VERTEX_POINT('',#14279);
#4106=VERTEX_POINT('',#14282);
#4107=VERTEX_POINT('',#14286);
#4108=VERTEX_POINT('',#14290);
#4109=VERTEX_POINT('',#14294);
#4110=VERTEX_POINT('',#14297);
#4111=VERTEX_POINT('',#14301);
#4112=VERTEX_POINT('',#14305);
#4113=VERTEX_POINT('',#14310);
#4114=VERTEX_POINT('',#14311);
#4115=VERTEX_POINT('',#14313);
#4116=VERTEX_POINT('',#14315);
#4117=VERTEX_POINT('',#14319);
#4118=VERTEX_POINT('',#14321);
#4119=VERTEX_POINT('',#14325);
#4120=VERTEX_POINT('',#14327);
#4121=VERTEX_POINT('',#14331);
#4122=VERTEX_POINT('',#14333);
#4123=VERTEX_POINT('',#14337);
#4124=VERTEX_POINT('',#14339);
#4956=EDGE_CURVE('',#4105,#4105,#3537,.T.);
#4957=EDGE_CURVE('',#4106,#4106,#3538,.T.);
#4958=EDGE_CURVE('',#4106,#4105,#2682,.T.);
#4959=EDGE_CURVE('',#4107,#4107,#3539,.T.);
#4960=EDGE_CURVE('',#4107,#4106,#2683,.T.);
#4961=EDGE_CURVE('',#4108,#4108,#3540,.T.);
#4962=EDGE_CURVE('',#4108,#4107,#2684,.T.);
#4963=EDGE_CURVE('',#4109,#4109,#3541,.T.);
#4964=EDGE_CURVE('',#4110,#4110,#3542,.F.);
#4965=EDGE_CURVE('',#4110,#4109,#2685,.T.);
#4966=EDGE_CURVE('',#4111,#4111,#3543,.F.);
#4967=EDGE_CURVE('',#4111,#4110,#2686,.T.);
#4968=EDGE_CURVE('',#4112,#4112,#3544,.T.);
#4969=EDGE_CURVE('',#4112,#4111,#2687,.T.);
#4970=EDGE_CURVE('',#4113,#4114,#2688,.T.);
#4971=EDGE_CURVE('',#4114,#4115,#2689,.T.);
#4972=EDGE_CURVE('',#4115,#4116,#2690,.T.);
#4973=EDGE_CURVE('',#4113,#4116,#2691,.T.);
#4974=EDGE_CURVE('',#4114,#4117,#2692,.T.);
#4975=EDGE_CURVE('',#4117,#4118,#2693,.T.);
#4976=EDGE_CURVE('',#4118,#4115,#2694,.T.);
#4977=EDGE_CURVE('',#4117,#4119,#2695,.T.);
#4978=EDGE_CURVE('',#4119,#4120,#2696,.T.);
#4979=EDGE_CURVE('',#4120,#4118,#2697,.T.);
#4980=EDGE_CURVE('',#4119,#4121,#2698,.T.);
#4981=EDGE_CURVE('',#4121,#4122,#2699,.T.);
#4982=EDGE_CURVE('',#4122,#4120,#2700,.T.);
#4983=EDGE_CURVE('',#4121,#4123,#2701,.T.);
#4984=EDGE_CURVE('',#4123,#4124,#2702,.T.);
#4985=EDGE_CURVE('',#4124,#4122,#2703,.T.);
#4986=EDGE_CURVE('',#4123,#4113,#2704,.T.);
#4987=EDGE_CURVE('',#4116,#4124,#2705,.T.);
#6650=ORIENTED_EDGE('',*,*,#4956,.F.);
#6651=ORIENTED_EDGE('',*,*,#4957,.F.);
#6652=ORIENTED_EDGE('',*,*,#4958,.T.);
#6653=ORIENTED_EDGE('',*,*,#4956,.T.);
#6654=ORIENTED_EDGE('',*,*,#4958,.F.);
#6655=ORIENTED_EDGE('',*,*,#4959,.F.);
#6656=ORIENTED_EDGE('',*,*,#4960,.T.);
#6657=ORIENTED_EDGE('',*,*,#4957,.T.);
#6658=ORIENTED_EDGE('',*,*,#4960,.F.);
#6659=ORIENTED_EDGE('',*,*,#4961,.F.);
#6660=ORIENTED_EDGE('',*,*,#4962,.T.);
#6661=ORIENTED_EDGE('',*,*,#4959,.T.);
#6662=ORIENTED_EDGE('',*,*,#4962,.F.);
#6663=ORIENTED_EDGE('',*,*,#4961,.T.);
#6664=ORIENTED_EDGE('',*,*,#4963,.F.);
#6665=ORIENTED_EDGE('',*,*,#4964,.F.);
#6666=ORIENTED_EDGE('',*,*,#4965,.T.);
#6667=ORIENTED_EDGE('',*,*,#4963,.T.);
#6668=ORIENTED_EDGE('',*,*,#4965,.F.);
#6669=ORIENTED_EDGE('',*,*,#4966,.F.);
#6670=ORIENTED_EDGE('',*,*,#4967,.T.);
#6671=ORIENTED_EDGE('',*,*,#4964,.T.);
#6672=ORIENTED_EDGE('',*,*,#4967,.F.);
#6673=ORIENTED_EDGE('',*,*,#4968,.F.);
#6674=ORIENTED_EDGE('',*,*,#4969,.T.);
#6675=ORIENTED_EDGE('',*,*,#4966,.T.);
#6676=ORIENTED_EDGE('',*,*,#4969,.F.);
#6677=ORIENTED_EDGE('',*,*,#4968,.T.);
#6678=ORIENTED_EDGE('',*,*,#4970,.T.);
#6679=ORIENTED_EDGE('',*,*,#4971,.T.);
#6680=ORIENTED_EDGE('',*,*,#4972,.T.);
#6681=ORIENTED_EDGE('',*,*,#4973,.F.);
#6682=ORIENTED_EDGE('',*,*,#4974,.T.);
#6683=ORIENTED_EDGE('',*,*,#4975,.T.);
#6684=ORIENTED_EDGE('',*,*,#4976,.T.);
#6685=ORIENTED_EDGE('',*,*,#4971,.F.);
#6686=ORIENTED_EDGE('',*,*,#4977,.T.);
#6687=ORIENTED_EDGE('',*,*,#4978,.T.);
#6688=ORIENTED_EDGE('',*,*,#4979,.T.);
#6689=ORIENTED_EDGE('',*,*,#4975,.F.);
#6690=ORIENTED_EDGE('',*,*,#4980,.T.);
#6691=ORIENTED_EDGE('',*,*,#4981,.T.);
#6692=ORIENTED_EDGE('',*,*,#4982,.T.);
#6693=ORIENTED_EDGE('',*,*,#4978,.F.);
#6694=ORIENTED_EDGE('',*,*,#4983,.T.);
#6695=ORIENTED_EDGE('',*,*,#4984,.T.);
#6696=ORIENTED_EDGE('',*,*,#4985,.T.);
#6697=ORIENTED_EDGE('',*,*,#4981,.F.);
#6698=ORIENTED_EDGE('',*,*,#4986,.T.);
#6699=ORIENTED_EDGE('',*,*,#4973,.T.);
#6700=ORIENTED_EDGE('',*,*,#4987,.T.);
#6701=ORIENTED_EDGE('',*,*,#4984,.F.);
#6702=ORIENTED_EDGE('',*,*,#4986,.F.);
#6703=ORIENTED_EDGE('',*,*,#4983,.F.);
#6704=ORIENTED_EDGE('',*,*,#4980,.F.);
#6705=ORIENTED_EDGE('',*,*,#4977,.F.);
#6706=ORIENTED_EDGE('',*,*,#4974,.F.);
#6707=ORIENTED_EDGE('',*,*,#4970,.F.);
#6708=ORIENTED_EDGE('',*,*,#4987,.F.);
#6709=ORIENTED_EDGE('',*,*,#4972,.F.);
#6710=ORIENTED_EDGE('',*,*,#4976,.F.);
#6711=ORIENTED_EDGE('',*,*,#4979,.F.);
#6712=ORIENTED_EDGE('',*,*,#4982,.F.);
#6713=ORIENTED_EDGE('',*,*,#4985,.F.);
#6904=CYLINDRICAL_SURFACE('',#8897,0.35);
#6905=CYLINDRICAL_SURFACE('',#8905,0.1954);
#7309=ADVANCED_FACE('',(#1604),#1190,.T.);
#7310=ADVANCED_FACE('',(#1605),#487,.T.);
#7311=ADVANCED_FACE('',(#1606),#6904,.T.);
#7312=ADVANCED_FACE('',(#1607),#488,.T.);
#7313=ADVANCED_FACE('',(#1608,#1005),#1191,.T.);
#7314=ADVANCED_FACE('',(#1609),#489,.T.);
#7315=ADVANCED_FACE('',(#1610),#6905,.T.);
#7316=ADVANCED_FACE('',(#1611),#490,.T.);
#7317=ADVANCED_FACE('',(#1612),#1192,.T.);
#7318=ADVANCED_FACE('',(#1613),#1193,.F.);
#7319=ADVANCED_FACE('',(#1614),#1194,.F.);
#7320=ADVANCED_FACE('',(#1615),#1195,.F.);
#7321=ADVANCED_FACE('',(#1616),#1196,.F.);
#7322=ADVANCED_FACE('',(#1617),#1197,.F.);
#7323=ADVANCED_FACE('',(#1618),#1198,.F.);
#7324=ADVANCED_FACE('',(#1619),#1199,.F.);
#7325=ADVANCED_FACE('',(#1620),#1200,.F.);
#7385=CLOSED_SHELL('',(#7309,#7310,#7311,#7312,#7313,#7314,#7315,#7316,
#7317));
#7386=CLOSED_SHELL('',(#7318,#7319,#7320,#7321,#7322,#7323,#7324,#7325));
#8892=AXIS2_PLACEMENT_3D('',#14277,#11248,#11249);
#8893=AXIS2_PLACEMENT_3D('',#14278,#11250,#11251);
#8894=AXIS2_PLACEMENT_3D('',#14280,#11252,#11253);
#8895=AXIS2_PLACEMENT_3D('',#14281,#11254,#11255);
#8896=AXIS2_PLACEMENT_3D('',#14283,#11256,#11257);
#8897=AXIS2_PLACEMENT_3D('',#14285,#11259,#11260);
#8898=AXIS2_PLACEMENT_3D('',#14287,#11261,#11262);
#8899=AXIS2_PLACEMENT_3D('',#14289,#11264,#11265);
#8900=AXIS2_PLACEMENT_3D('',#14291,#11266,#11267);
#8901=AXIS2_PLACEMENT_3D('',#14293,#11269,#11270);
#8902=AXIS2_PLACEMENT_3D('',#14295,#11271,#11272);
#8903=AXIS2_PLACEMENT_3D('',#14296,#11273,#11274);
#8904=AXIS2_PLACEMENT_3D('',#14298,#11275,#11276);
#8905=AXIS2_PLACEMENT_3D('',#14300,#11278,#11279);
#8906=AXIS2_PLACEMENT_3D('',#14302,#11280,#11281);
#8907=AXIS2_PLACEMENT_3D('',#14304,#11283,#11284);
#8908=AXIS2_PLACEMENT_3D('',#14306,#11285,#11286);
#8909=AXIS2_PLACEMENT_3D('',#14308,#11288,#11289);
#8910=AXIS2_PLACEMENT_3D('',#14309,#11290,#11291);
#8911=AXIS2_PLACEMENT_3D('',#14318,#11296,#11297);
#8912=AXIS2_PLACEMENT_3D('',#14324,#11301,#11302);
#8913=AXIS2_PLACEMENT_3D('',#14330,#11306,#11307);
#8914=AXIS2_PLACEMENT_3D('',#14336,#11311,#11312);
#8915=AXIS2_PLACEMENT_3D('',#14342,#11316,#11317);
#8916=AXIS2_PLACEMENT_3D('',#14345,#11320,#11321);
#8917=AXIS2_PLACEMENT_3D('',#14346,#11322,#11323);
#11248=DIRECTION('axis',(0.,0.,1.));
#11249=DIRECTION('refdir',(1.,0.,0.));
#11250=DIRECTION('center_axis',(0.,1.,0.));
#11251=DIRECTION('ref_axis',(0.,0.,1.));
#11252=DIRECTION('center_axis',(0.,-1.,0.));
#11253=DIRECTION('ref_axis',(1.,0.,0.));
#11254=DIRECTION('center_axis',(0.,-1.,0.));
#11255=DIRECTION('ref_axis',(1.,0.,0.));
#11256=DIRECTION('center_axis',(0.,-1.,0.));
#11257=DIRECTION('ref_axis',(1.,0.,0.));
#11258=DIRECTION('',(0.707106781186547,0.707106781186548,8.65956056235493E-17));
#11259=DIRECTION('center_axis',(0.,-1.,0.));
#11260=DIRECTION('ref_axis',(1.,0.,0.));
#11261=DIRECTION('center_axis',(0.,-1.,0.));
#11262=DIRECTION('ref_axis',(1.,0.,0.));
#11263=DIRECTION('',(0.,1.,0.));
#11264=DIRECTION('center_axis',(0.,1.,0.));
#11265=DIRECTION('ref_axis',(1.,0.,0.));
#11266=DIRECTION('center_axis',(0.,-1.,0.));
#11267=DIRECTION('ref_axis',(1.,0.,0.));
#11268=DIRECTION('',(-0.707106781186547,0.707106781186548,-8.65956056235493E-17));
#11269=DIRECTION('center_axis',(0.,-1.,0.));
#11270=DIRECTION('ref_axis',(0.,0.,-1.));
#11271=DIRECTION('center_axis',(0.,-1.,0.));
#11272=DIRECTION('ref_axis',(1.,0.,0.));
#11273=DIRECTION('center_axis',(0.,1.,0.));
#11274=DIRECTION('ref_axis',(1.,0.,0.));
#11275=DIRECTION('center_axis',(0.,1.,0.));
#11276=DIRECTION('ref_axis',(1.,0.,0.));
#11277=DIRECTION('',(-0.447213595499958,0.894427190999916,-5.47678698264203E-17));
#11278=DIRECTION('center_axis',(0.,-1.,0.));
#11279=DIRECTION('ref_axis',(1.,0.,0.));
#11280=DIRECTION('center_axis',(0.,1.,0.));
#11281=DIRECTION('ref_axis',(1.,0.,0.));
#11282=DIRECTION('',(0.,1.,0.));
#11283=DIRECTION('center_axis',(0.,1.,0.));
#11284=DIRECTION('ref_axis',(1.,0.,0.));
#11285=DIRECTION('center_axis',(0.,-1.,0.));
#11286=DIRECTION('ref_axis',(1.,0.,0.));
#11287=DIRECTION('',(-0.707106781186547,0.707106781186548,-8.65956056235493E-17));
#11288=DIRECTION('center_axis',(0.,-1.,0.));
#11289=DIRECTION('ref_axis',(0.,0.,-1.));
#11290=DIRECTION('center_axis',(0.866025403784439,0.,-0.5));
#11291=DIRECTION('ref_axis',(0.5,0.,0.866025403784439));
#11292=DIRECTION('',(-0.5,0.,-0.866025403784439));
#11293=DIRECTION('',(0.,-1.,0.));
#11294=DIRECTION('',(0.5,0.,0.866025403784439));
#11295=DIRECTION('',(0.,-1.,0.));
#11296=DIRECTION('center_axis',(1.60246890531964E-16,0.,-1.));
#11297=DIRECTION('ref_axis',(1.,0.,1.60246890531964E-16));
#11298=DIRECTION('',(-1.,0.,-1.60246890531964E-16));
#11299=DIRECTION('',(0.,-1.,0.));
#11300=DIRECTION('',(1.,0.,1.60246890531964E-16));
#11301=DIRECTION('center_axis',(-0.866025403784439,0.,-0.5));
#11302=DIRECTION('ref_axis',(0.5,0.,-0.866025403784439));
#11303=DIRECTION('',(-0.5,0.,0.866025403784439));
#11304=DIRECTION('',(0.,-1.,0.));
#11305=DIRECTION('',(0.5,0.,-0.866025403784439));
#11306=DIRECTION('center_axis',(-0.866025403784439,0.,0.5));
#11307=DIRECTION('ref_axis',(-0.5,0.,-0.866025403784439));
#11308=DIRECTION('',(0.5,0.,0.866025403784439));
#11309=DIRECTION('',(0.,-1.,0.));
#11310=DIRECTION('',(-0.5,0.,-0.866025403784439));
#11311=DIRECTION('center_axis',(-1.60246890531964E-16,0.,1.));
#11312=DIRECTION('ref_axis',(-1.,0.,-1.60246890531964E-16));
#11313=DIRECTION('',(1.,0.,1.60246890531964E-16));
#11314=DIRECTION('',(0.,-1.,0.));
#11315=DIRECTION('',(-1.,0.,-1.60246890531964E-16));
#11316=DIRECTION('center_axis',(0.866025403784439,0.,0.5));
#11317=DIRECTION('ref_axis',(-0.5,0.,0.866025403784439));
#11318=DIRECTION('',(0.5,0.,-0.866025403784439));
#11319=DIRECTION('',(-0.5,0.,0.866025403784439));
#11320=DIRECTION('center_axis',(0.,1.,0.));
#11321=DIRECTION('ref_axis',(1.,0.,0.));
#11322=DIRECTION('center_axis',(0.,-1.,0.));
#11323=DIRECTION('ref_axis',(0.,0.,-1.));
#14277=CARTESIAN_POINT('',(0.,0.,0.));
#14278=CARTESIAN_POINT('Origin',(0.3,0.4,0.));
#14279=CARTESIAN_POINT('',(-0.3,0.4,-3.67394039744206E-17));
#14280=CARTESIAN_POINT('Origin',(0.,0.4,0.));
#14281=CARTESIAN_POINT('Origin',(0.,0.375,0.));
#14282=CARTESIAN_POINT('',(-0.35,0.35,-4.28626379701573E-17));
#14283=CARTESIAN_POINT('Origin',(0.,0.35,0.));
#14284=CARTESIAN_POINT('',(-0.325,0.375,-3.9801020972289E-17));
#14285=CARTESIAN_POINT('Origin',(0.,0.19,0.));
#14286=CARTESIAN_POINT('',(-0.35,0.03,-4.28626379701574E-17));
#14287=CARTESIAN_POINT('Origin',(0.,0.03,0.));
#14288=CARTESIAN_POINT('',(-0.35,0.19,-4.28626379701574E-17));
#14289=CARTESIAN_POINT('Origin',(0.,0.0149999999999999,0.));
#14290=CARTESIAN_POINT('',(-0.32,-3.29597460435593E-17,-3.91886975727153E-17));
#14291=CARTESIAN_POINT('Origin',(0.,0.,0.));
#14292=CARTESIAN_POINT('',(-0.335,0.0149999999999999,-4.10256677714363E-17));
#14293=CARTESIAN_POINT('Origin',(0.22,0.,0.));
#14294=CARTESIAN_POINT('',(-0.22,-6.93889390390723E-18,-2.69422295812418E-17));
#14295=CARTESIAN_POINT('Origin',(0.,0.,0.));
#14296=CARTESIAN_POINT('Origin',(0.,-0.02,0.));
#14297=CARTESIAN_POINT('',(-0.1954,-0.0492,2.39295984553393E-17));
#14298=CARTESIAN_POINT('Origin',(0.,-0.0492,0.));
#14299=CARTESIAN_POINT('',(-0.21,-0.02,-2.57175827820944E-17));
#14300=CARTESIAN_POINT('Origin',(0.,-0.8,0.));
#14301=CARTESIAN_POINT('',(-0.1954,-1.5646,2.39295984553393E-17));
#14302=CARTESIAN_POINT('Origin',(0.,-1.5646,0.));
#14303=CARTESIAN_POINT('',(-0.1954,-0.8,-2.39295984553393E-17));
#14304=CARTESIAN_POINT('Origin',(0.,-1.58,0.));
#14305=CARTESIAN_POINT('',(-0.16,-1.6,-1.95943487863577E-17));
#14306=CARTESIAN_POINT('Origin',(0.,-1.6,0.));
#14307=CARTESIAN_POINT('',(-0.18,-1.58,-2.20436423846524E-17));
#14308=CARTESIAN_POINT('Origin',(0.,-1.6,0.));
#14309=CARTESIAN_POINT('Origin',(0.0866025403784439,-0.4,-0.15));
#14310=CARTESIAN_POINT('',(0.173205080756888,-0.4,0.));
#14311=CARTESIAN_POINT('',(0.0866025403784439,-0.4,-0.15));
#14312=CARTESIAN_POINT('',(0.173205080756888,-0.4,0.));
#14313=CARTESIAN_POINT('',(0.0866025403784439,-0.64,-0.15));
#14314=CARTESIAN_POINT('',(0.0866025403784439,-0.4,-0.15));
#14315=CARTESIAN_POINT('',(0.173205080756888,-0.64,0.));
#14316=CARTESIAN_POINT('',(0.173205080756888,-0.64,0.));
#14317=CARTESIAN_POINT('',(0.173205080756888,-0.4,0.));
#14318=CARTESIAN_POINT('Origin',(-0.0866025403784438,-0.4,-0.15));
#14319=CARTESIAN_POINT('',(-0.0866025403784438,-0.4,-0.15));
#14320=CARTESIAN_POINT('',(0.0866025403784439,-0.4,-0.15));
#14321=CARTESIAN_POINT('',(-0.0866025403784438,-0.64,-0.15));
#14322=CARTESIAN_POINT('',(-0.0866025403784438,-0.4,-0.15));
#14323=CARTESIAN_POINT('',(0.0866025403784439,-0.64,-0.15));
#14324=CARTESIAN_POINT('Origin',(-0.173205080756888,-0.4,-2.77555756156289E-17));
#14325=CARTESIAN_POINT('',(-0.173205080756888,-0.4,-2.12115047744981E-17));
#14326=CARTESIAN_POINT('',(-0.0866025403784438,-0.4,-0.15));
#14327=CARTESIAN_POINT('',(-0.173205080756888,-0.64,-2.77555756156289E-17));
#14328=CARTESIAN_POINT('',(-0.173205080756888,-0.4,-2.12115047744981E-17));
#14329=CARTESIAN_POINT('',(-0.0866025403784438,-0.64,-0.15));
#14330=CARTESIAN_POINT('Origin',(-0.0866025403784439,-0.4,0.15));
#14331=CARTESIAN_POINT('',(-0.0866025403784439,-0.4,0.15));
#14332=CARTESIAN_POINT('',(-0.173205080756888,-0.4,-2.12115047744981E-17));
#14333=CARTESIAN_POINT('',(-0.0866025403784439,-0.64,0.15));
#14334=CARTESIAN_POINT('',(-0.0866025403784439,-0.4,0.15));
#14335=CARTESIAN_POINT('',(-0.173205080756888,-0.64,-2.12115047744981E-17));
#14336=CARTESIAN_POINT('Origin',(0.0866025403784439,-0.4,0.15));
#14337=CARTESIAN_POINT('',(0.0866025403784439,-0.4,0.15));
#14338=CARTESIAN_POINT('',(-0.0866025403784439,-0.4,0.15));
#14339=CARTESIAN_POINT('',(0.0866025403784439,-0.64,0.15));
#14340=CARTESIAN_POINT('',(0.0866025403784439,-0.4,0.15));
#14341=CARTESIAN_POINT('',(-0.0866025403784439,-0.64,0.15));
#14342=CARTESIAN_POINT('Origin',(0.173205080756888,-0.4,0.));
#14343=CARTESIAN_POINT('',(0.0866025403784439,-0.4,0.15));
#14344=CARTESIAN_POINT('',(0.0866025403784439,-0.64,0.15));
#14345=CARTESIAN_POINT('Origin',(0.,-0.4,-2.77555756156289E-17));
#14346=CARTESIAN_POINT('Origin',(0.,-0.64,-2.77555756156289E-17));
#14454=UNCERTAINTY_MEASURE_WITH_UNIT(LENGTH_MEASURE(0.001),#14513,
'DISTANCE_ACCURACY_VALUE',
'Maximum model space distance between geometric entities at asserted c
onnectivities');
#14455=UNCERTAINTY_MEASURE_WITH_UNIT(LENGTH_MEASURE(0.001),#14513,
'DISTANCE_ACCURACY_VALUE',
'Maximum model space distance between geometric entities at asserted c
onnectivities');
#14511=(
GEOMETRIC_REPRESENTATION_CONTEXT(3)
GLOBAL_UNCERTAINTY_ASSIGNED_CONTEXT((#14454))
GLOBAL_UNIT_ASSIGNED_CONTEXT((#14513,#14515,#14516))
REPRESENTATION_CONTEXT('','3D')
);
#14512=(
GEOMETRIC_REPRESENTATION_CONTEXT(3)
GLOBAL_UNCERTAINTY_ASSIGNED_CONTEXT((#14455))
GLOBAL_UNIT_ASSIGNED_CONTEXT((#14513,#14515,#14516))
REPRESENTATION_CONTEXT('','3D')
);
#14513=(
LENGTH_UNIT()
NAMED_UNIT(*)
SI_UNIT(.CENTI.,.METRE.)
);
#14515=(
NAMED_UNIT(*)
PLANE_ANGLE_UNIT()
SI_UNIT($,.RADIAN.)
);
#14516=(
NAMED_UNIT(*)
SI_UNIT($,.STERADIAN.)
SOLID_ANGLE_UNIT()
);
#14572=SHAPE_DEFINITION_REPRESENTATION(#14688,#14796);
#14688=PRODUCT_DEFINITION_SHAPE('',$,#14853);
#14796=SHAPE_REPRESENTATION('',(#8892),#14511);
#14797=PRODUCT_DEFINITION_CONTEXT('part definition',#14967,'design');
#14853=PRODUCT_DEFINITION('Cap Screw - M4x16','Cap Screw - M4x16',#14909,
#14797);
#14909=PRODUCT_DEFINITION_FORMATION('',$,#15024);
#14967=APPLICATION_CONTEXT(
'Core Data for Automotive Mechanical Design Process');
#14968=PRODUCT_CONTEXT('part definition',#14967,'mechanical');
#15024=PRODUCT('Cap Screw - M4x16','Cap Screw - M4x16',
'Cap Screw - M4x16',(#14968));
#15088=COLOUR_RGB('Black',0.12,0.14,0.17);
#15089=FILL_AREA_STYLE_COLOUR('',#15088);
#15090=FILL_AREA_STYLE('',(#15089));
#15091=SURFACE_STYLE_FILL_AREA(#15090);
#15092=SURFACE_SIDE_STYLE('',(#15091));
#15093=SURFACE_STYLE_USAGE(.BOTH.,#15092);
#15094=PRESENTATION_STYLE_ASSIGNMENT((#15093));
ENDSEC;
END-ISO-10303-21;
